ISO-10303-21;
HEADER;
/* Generated by software containing ST-Developer
 * from STEP Tools, Inc. (www.steptools.com) 
 */

FILE_DESCRIPTION(
/* description */ ('Four-bar parallelogram arm'),
/* implementation_level */ '2;1');

FILE_NAME(
/* name */ 'Front spacer (2).step',
/* time_stamp */ '2026-10-28T03:24:55-07:00',
/* author */ (''),
/* organization */ (''),
/* preprocessor_version */ 'ST-DEVELOPER v20.2',
/* originating_system */ 'Autodesk Translation Framework v15.17.0.0',
/* authorisation */ '');

FILE_SCHEMA (('AUTOMOTIVE_DESIGN { 1 0 10303 214 3 1 1 }'));
ENDSEC;

DATA;
#10=MECHANICAL_DESIGN_GEOMETRIC_PRESENTATION_REPRESENTATION('',(#677),#14512);
#569=SHAPE_REPRESENTATION_RELATIONSHIP('SRR','None',#14794,#619);
#619=ADVANCED_BREP_SHAPE_REPRESENTATION('',(#733),#14509);
#677=STYLED_ITEM('',(#15080),#733);
#733=MANIFOLD_SOLID_BREP('Body1',#7383);
#1001=FACE_BOUND('',#2285,.T.);
#1002=FACE_BOUND('',#2287,.T.);
#1186=PLANE('',#8881);
#1187=PLANE('',#8882);
#1596=FACE_OUTER_BOUND('',#2282,.T.);
#1597=FACE_OUTER_BOUND('',#2283,.T.);
#1598=FACE_OUTER_BOUND('',#2284,.T.);
#1599=FACE_OUTER_BOUND('',#2286,.T.);
#2282=EDGE_LOOP('',(#6626,#6627,#6628,#6629));
#2283=EDGE_LOOP('',(#6630,#6631,#6632,#6633));
#2284=EDGE_LOOP('',(#6634));
#2285=EDGE_LOOP('',(#6635));
#2286=EDGE_LOOP('',(#6636));
#2287=EDGE_LOOP('',(#6637));
#2678=LINE('',#14252,#3072);
#2679=LINE('',#14258,#3073);
#3072=VECTOR('',#11214,0.504999999999999);
#3073=VECTOR('',#11221,0.699999999999999);
#3529=CIRCLE('',#8876,0.504999999999999);
#3530=CIRCLE('',#8877,0.504999999999999);
#3531=CIRCLE('',#8879,0.699999999999999);
#3532=CIRCLE('',#8880,0.699999999999999);
#4097=VERTEX_POINT('',#14249);
#4098=VERTEX_POINT('',#14251);
#4099=VERTEX_POINT('',#14255);
#4100=VERTEX_POINT('',#14257);
#4944=EDGE_CURVE('',#4097,#4097,#3529,.T.);
#4945=EDGE_CURVE('',#4097,#4098,#2678,.T.);
#4946=EDGE_CURVE('',#4098,#4098,#3530,.T.);
#4947=EDGE_CURVE('',#4099,#4099,#3531,.T.);
#4948=EDGE_CURVE('',#4099,#4100,#2679,.T.);
#4949=EDGE_CURVE('',#4100,#4100,#3532,.T.);
#6626=ORIENTED_EDGE('',*,*,#4944,.F.);
#6627=ORIENTED_EDGE('',*,*,#4945,.T.);
#6628=ORIENTED_EDGE('',*,*,#4946,.T.);
#6629=ORIENTED_EDGE('',*,*,#4945,.F.);
#6630=ORIENTED_EDGE('',*,*,#4947,.F.);
#6631=ORIENTED_EDGE('',*,*,#4948,.T.);
#6632=ORIENTED_EDGE('',*,*,#4949,.T.);
#6633=ORIENTED_EDGE('',*,*,#4948,.F.);
#6634=ORIENTED_EDGE('',*,*,#4947,.T.);
#6635=ORIENTED_EDGE('',*,*,#4944,.T.);
#6636=ORIENTED_EDGE('',*,*,#4949,.F.);
#6637=ORIENTED_EDGE('',*,*,#4946,.F.);
#6900=CYLINDRICAL_SURFACE('',#8875,0.504999999999999);
#6901=CYLINDRICAL_SURFACE('',#8878,0.699999999999999);
#7301=ADVANCED_FACE('',(#1596),#6900,.F.);
#7302=ADVANCED_FACE('',(#1597),#6901,.T.);
#7303=ADVANCED_FACE('',(#1598,#1001),#1186,.T.);
#7304=ADVANCED_FACE('',(#1599,#1002),#1187,.F.);
#7383=CLOSED_SHELL('',(#7301,#7302,#7303,#7304));
#8874=AXIS2_PLACEMENT_3D('',#14247,#11208,#11209);
#8875=AXIS2_PLACEMENT_3D('',#14248,#11210,#11211);
#8876=AXIS2_PLACEMENT_3D('',#14250,#11212,#11213);
#8877=AXIS2_PLACEMENT_3D('',#14253,#11215,#11216);
#8878=AXIS2_PLACEMENT_3D('',#14254,#11217,#11218);
#8879=AXIS2_PLACEMENT_3D('',#14256,#11219,#11220);
#8880=AXIS2_PLACEMENT_3D('',#14259,#11222,#11223);
#8881=AXIS2_PLACEMENT_3D('',#14260,#11224,#11225);
#8882=AXIS2_PLACEMENT_3D('',#14261,#11226,#11227);
#11208=DIRECTION('axis',(0.,0.,1.));
#11209=DIRECTION('refdir',(1.,0.,0.));
#11210=DIRECTION('center_axis',(0.,1.,0.));
#11211=DIRECTION('ref_axis',(1.,0.,0.));
#11212=DIRECTION('center_axis',(0.,-1.,0.));
#11213=DIRECTION('ref_axis',(1.,0.,0.));
#11214=DIRECTION('',(0.,-1.,0.));
#11215=DIRECTION('center_axis',(0.,-1.,0.));
#11216=DIRECTION('ref_axis',(1.,0.,0.));
#11217=DIRECTION('center_axis',(0.,1.,0.));
#11218=DIRECTION('ref_axis',(1.,0.,0.));
#11219=DIRECTION('center_axis',(0.,1.,0.));
#11220=DIRECTION('ref_axis',(1.,0.,0.));
#11221=DIRECTION('',(0.,-1.,0.));
#11222=DIRECTION('center_axis',(0.,1.,0.));
#11223=DIRECTION('ref_axis',(1.,0.,0.));
#11224=DIRECTION('center_axis',(0.,1.,0.));
#11225=DIRECTION('ref_axis',(1.,0.,0.));
#11226=DIRECTION('center_axis',(0.,1.,0.));
#11227=DIRECTION('ref_axis',(1.,0.,0.));
#14247=CARTESIAN_POINT('',(0.,0.,0.));
#14248=CARTESIAN_POINT('Origin',(20.,-1.6,14.));
#14249=CARTESIAN_POINT('',(19.495,-1.05,14.));
#14250=CARTESIAN_POINT('Origin',(20.,-1.05,14.));
#14251=CARTESIAN_POINT('',(19.495,-1.6,14.));
#14252=CARTESIAN_POINT('',(19.495,-1.6,14.));
#14253=CARTESIAN_POINT('Origin',(20.,-1.6,14.));
#14254=CARTESIAN_POINT('Origin',(20.,-1.6,14.));
#14255=CARTESIAN_POINT('',(19.3,-1.05,14.));
#14256=CARTESIAN_POINT('Origin',(20.,-1.05,14.));
#14257=CARTESIAN_POINT('',(19.3,-1.6,14.));
#14258=CARTESIAN_POINT('',(19.3,-1.6,14.));
#14259=CARTESIAN_POINT('Origin',(20.,-1.6,14.));
#14260=CARTESIAN_POINT('Origin',(20.,-1.05,14.));
#14261=CARTESIAN_POINT('Origin',(20.,-1.6,14.));
#14452=UNCERTAINTY_MEASURE_WITH_UNIT(LENGTH_MEASURE(0.001),#14513,
'DISTANCE_ACCURACY_VALUE',
'Maximum model space distance between geometric entities at asserted c
onnectivities');
#14455=UNCERTAINTY_MEASURE_WITH_UNIT(LENGTH_MEASURE(0.001),#14513,
'DISTANCE_ACCURACY_VALUE',
'Maximum model space distance between geometric entities at asserted c
onnectivities');
#14509=(
GEOMETRIC_REPRESENTATION_CONTEXT(3)
GLOBAL_UNCERTAINTY_ASSIGNED_CONTEXT((#14452))
GLOBAL_UNIT_ASSIGNED_CONTEXT((#14513,#14515,#14516))
REPRESENTATION_CONTEXT('','3D')
);
#14512=(
GEOMETRIC_REPRESENTATION_CONTEXT(3)
GLOBAL_UNCERTAINTY_ASSIGNED_CONTEXT((#14455))
GLOBAL_UNIT_ASSIGNED_CONTEXT((#14513,#14515,#14516))
REPRESENTATION_CONTEXT('','3D')
);
#14513=(
LENGTH_UNIT()
NAMED_UNIT(*)
SI_UNIT(.CENTI.,.METRE.)
);
#14515=(
NAMED_UNIT(*)
PLANE_ANGLE_UNIT()
SI_UNIT($,.RADIAN.)
);
#14516=(
NAMED_UNIT(*)
SI_UNIT($,.STERADIAN.)
SOLID_ANGLE_UNIT()
);
#14570=SHAPE_DEFINITION_REPRESENTATION(#14686,#14794);
#14686=PRODUCT_DEFINITION_SHAPE('',$,#14851);
#14794=SHAPE_REPRESENTATION('',(#8874),#14509);
#14797=PRODUCT_DEFINITION_CONTEXT('part definition',#14967,'design');
#14851=PRODUCT_DEFINITION('Front spacer (2)','Front spacer (2)',#14907,#14797);
#14907=PRODUCT_DEFINITION_FORMATION('',$,#15022);
#14967=APPLICATION_CONTEXT(
'Core Data for Automotive Mechanical Design Process');
#14968=PRODUCT_CONTEXT('part definition',#14967,'mechanical');
#15022=PRODUCT('Front spacer (2)','Front spacer (2)','Front spacer (2)',(#14968));
#15074=COLOUR_RGB('Sky Blue',0.24,0.69,0.87);
#15075=FILL_AREA_STYLE_COLOUR('',#15074);
#15076=FILL_AREA_STYLE('',(#15075));
#15077=SURFACE_STYLE_FILL_AREA(#15076);
#15078=SURFACE_SIDE_STYLE('',(#15077));
#15079=SURFACE_STYLE_USAGE(.BOTH.,#15078);
#15080=PRESENTATION_STYLE_ASSIGNMENT((#15079));
ENDSEC;
END-ISO-10303-21;
